ISO-10303-21;
HEADER;
/* Generated by software containing ST-Developer
 * from STEP Tools, Inc. (www.steptools.com) 
 */

FILE_DESCRIPTION(
/* description */ ('PAT-091'),
/* implementation_level */ '2;1');

FILE_NAME(
/* name */ 'Linear bearing keeper (1).step',
/* time_stamp */ '2026-10-27T15:34:44-07:00',
/* author */ (''),
/* organization */ (''),
/* preprocessor_version */ 'ST-DEVELOPER v20.2',
/* originating_system */ 'Autodesk Translation Framework v15.17.0.0',
/* authorisation */ '');

FILE_SCHEMA (('AUTOMOTIVE_DESIGN { 1 0 10303 214 3 1 1 }'));
ENDSEC;

DATA;
#10=MECHANICAL_DESIGN_GEOMETRIC_PRESENTATION_REPRESENTATION('',(#1004),#25100);
#784=SHAPE_REPRESENTATION_RELATIONSHIP('SRR','None',#25547,#894);
#894=ADVANCED_BREP_SHAPE_REPRESENTATION('',(#1126),#25017);
#1004=STYLED_ITEM('',(#26191),#1126);
#1126=MANIFOLD_SOLID_BREP('Body1',#13283);
#1406=FACE_BOUND('',#3356,.T.);
#1407=FACE_BOUND('',#3359,.T.);
#1408=FACE_BOUND('',#3368,.T.);
#1409=FACE_BOUND('',#3369,.T.);
#1410=FACE_BOUND('',#3370,.T.);
#1411=FACE_BOUND('',#3372,.T.);
#1412=FACE_BOUND('',#3373,.T.);
#1413=FACE_BOUND('',#3374,.T.);
#1791=PLANE('',#15163);
#1792=PLANE('',#15168);
#1793=PLANE('',#15177);
#1794=PLANE('',#15178);
#1795=PLANE('',#15179);
#1796=PLANE('',#15180);
#1797=PLANE('',#15181);
#1798=PLANE('',#15182);
#2345=FACE_OUTER_BOUND('',#3354,.T.);
#2346=FACE_OUTER_BOUND('',#3355,.T.);
#2347=FACE_OUTER_BOUND('',#3357,.T.);
#2348=FACE_OUTER_BOUND('',#3358,.T.);
#2349=FACE_OUTER_BOUND('',#3360,.T.);
#2350=FACE_OUTER_BOUND('',#3361,.T.);
#2351=FACE_OUTER_BOUND('',#3362,.T.);
#2352=FACE_OUTER_BOUND('',#3363,.T.);
#2353=FACE_OUTER_BOUND('',#3364,.T.);
#2354=FACE_OUTER_BOUND('',#3365,.T.);
#2355=FACE_OUTER_BOUND('',#3366,.T.);
#2356=FACE_OUTER_BOUND('',#3367,.T.);
#2357=FACE_OUTER_BOUND('',#3371,.T.);
#3354=EDGE_LOOP('',(#10152,#10153,#10154,#10155));
#3355=EDGE_LOOP('',(#10156));
#3356=EDGE_LOOP('',(#10157));
#3357=EDGE_LOOP('',(#10158,#10159,#10160,#10161));
#3358=EDGE_LOOP('',(#10162));
#3359=EDGE_LOOP('',(#10163));
#3360=EDGE_LOOP('',(#10164,#10165,#10166,#10167));
#3361=EDGE_LOOP('',(#10168,#10169,#10170,#10171));
#3362=EDGE_LOOP('',(#10172,#10173,#10174,#10175));
#3363=EDGE_LOOP('',(#10176,#10177,#10178,#10179));
#3364=EDGE_LOOP('',(#10180,#10181,#10182,#10183));
#3365=EDGE_LOOP('',(#10184,#10185,#10186,#10187));
#3366=EDGE_LOOP('',(#10188,#10189,#10190,#10191));
#3367=EDGE_LOOP('',(#10192,#10193,#10194,#10195));
#3368=EDGE_LOOP('',(#10196));
#3369=EDGE_LOOP('',(#10197));
#3370=EDGE_LOOP('',(#10198));
#3371=EDGE_LOOP('',(#10199,#10200,#10201,#10202));
#3372=EDGE_LOOP('',(#10203));
#3373=EDGE_LOOP('',(#10204));
#3374=EDGE_LOOP('',(#10205));
#4459=LINE('',#22279,#5199);
#4460=LINE('',#22288,#5200);
#4461=LINE('',#22297,#5201);
#4462=LINE('',#22301,#5202);
#4463=LINE('',#22305,#5203);
#4464=LINE('',#22310,#5204);
#4465=LINE('',#22312,#5205);
#4466=LINE('',#22314,#5206);
#4467=LINE('',#22315,#5207);
#4468=LINE('',#22318,#5208);
#4469=LINE('',#22320,#5209);
#4470=LINE('',#22321,#5210);
#4471=LINE('',#22324,#5211);
#4472=LINE('',#22326,#5212);
#4473=LINE('',#22327,#5213);
#4474=LINE('',#22329,#5214);
#4475=LINE('',#22330,#5215);
#5199=VECTOR('',#17957,1.04);
#5200=VECTOR('',#17968,1.04);
#5201=VECTOR('',#17979,0.65);
#5202=VECTOR('',#17984,0.8);
#5203=VECTOR('',#17989,0.8);
#5204=VECTOR('',#17994,1.);
#5205=VECTOR('',#17995,1.);
#5206=VECTOR('',#17996,1.);
#5207=VECTOR('',#17997,1.);
#5208=VECTOR('',#18000,1.);
#5209=VECTOR('',#18001,1.);
#5210=VECTOR('',#18002,1.);
#5211=VECTOR('',#18005,1.);
#5212=VECTOR('',#18006,1.);
#5213=VECTOR('',#18007,1.);
#5214=VECTOR('',#18010,1.);
#5215=VECTOR('',#18011,1.);
#5859=CIRCLE('',#15161,1.04);
#5860=CIRCLE('',#15162,1.04);
#5861=CIRCLE('',#15164,0.8);
#5862=CIRCLE('',#15166,1.04);
#5863=CIRCLE('',#15167,1.04);
#5864=CIRCLE('',#15169,0.8);
#5865=CIRCLE('',#15171,0.65);
#5866=CIRCLE('',#15172,0.65);
#5867=CIRCLE('',#15174,0.8);
#5868=CIRCLE('',#15176,0.8);
#6774=VERTEX_POINT('',#22276);
#6775=VERTEX_POINT('',#22278);
#6776=VERTEX_POINT('',#22282);
#6777=VERTEX_POINT('',#22285);
#6778=VERTEX_POINT('',#22287);
#6779=VERTEX_POINT('',#22291);
#6780=VERTEX_POINT('',#22294);
#6781=VERTEX_POINT('',#22296);
#6782=VERTEX_POINT('',#22300);
#6783=VERTEX_POINT('',#22304);
#6784=VERTEX_POINT('',#22308);
#6785=VERTEX_POINT('',#22309);
#6786=VERTEX_POINT('',#22311);
#6787=VERTEX_POINT('',#22313);
#6788=VERTEX_POINT('',#22317);
#6789=VERTEX_POINT('',#22319);
#6790=VERTEX_POINT('',#22323);
#6791=VERTEX_POINT('',#22325);
#8011=EDGE_CURVE('',#6774,#6774,#5859,.T.);
#8012=EDGE_CURVE('',#6774,#6775,#4459,.T.);
#8013=EDGE_CURVE('',#6775,#6775,#5860,.T.);
#8014=EDGE_CURVE('',#6776,#6776,#5861,.T.);
#8015=EDGE_CURVE('',#6777,#6777,#5862,.T.);
#8016=EDGE_CURVE('',#6777,#6778,#4460,.T.);
#8017=EDGE_CURVE('',#6778,#6778,#5863,.T.);
#8018=EDGE_CURVE('',#6779,#6779,#5864,.T.);
#8019=EDGE_CURVE('',#6780,#6780,#5865,.T.);
#8020=EDGE_CURVE('',#6780,#6781,#4461,.T.);
#8021=EDGE_CURVE('',#6781,#6781,#5866,.T.);
#8022=EDGE_CURVE('',#6779,#6782,#4462,.T.);
#8023=EDGE_CURVE('',#6782,#6782,#5867,.T.);
#8024=EDGE_CURVE('',#6776,#6783,#4463,.T.);
#8025=EDGE_CURVE('',#6783,#6783,#5868,.T.);
#8026=EDGE_CURVE('',#6784,#6785,#4464,.T.);
#8027=EDGE_CURVE('',#6785,#6786,#4465,.T.);
#8028=EDGE_CURVE('',#6787,#6786,#4466,.T.);
#8029=EDGE_CURVE('',#6784,#6787,#4467,.T.);
#8030=EDGE_CURVE('',#6788,#6784,#4468,.T.);
#8031=EDGE_CURVE('',#6789,#6787,#4469,.T.);
#8032=EDGE_CURVE('',#6788,#6789,#4470,.T.);
#8033=EDGE_CURVE('',#6790,#6788,#4471,.T.);
#8034=EDGE_CURVE('',#6791,#6789,#4472,.T.);
#8035=EDGE_CURVE('',#6790,#6791,#4473,.T.);
#8036=EDGE_CURVE('',#6785,#6790,#4474,.T.);
#8037=EDGE_CURVE('',#6786,#6791,#4475,.T.);
#10152=ORIENTED_EDGE('',*,*,#8011,.F.);
#10153=ORIENTED_EDGE('',*,*,#8012,.T.);
#10154=ORIENTED_EDGE('',*,*,#8013,.T.);
#10155=ORIENTED_EDGE('',*,*,#8012,.F.);
#10156=ORIENTED_EDGE('',*,*,#8013,.F.);
#10157=ORIENTED_EDGE('',*,*,#8014,.F.);
#10158=ORIENTED_EDGE('',*,*,#8015,.F.);
#10159=ORIENTED_EDGE('',*,*,#8016,.T.);
#10160=ORIENTED_EDGE('',*,*,#8017,.T.);
#10161=ORIENTED_EDGE('',*,*,#8016,.F.);
#10162=ORIENTED_EDGE('',*,*,#8017,.F.);
#10163=ORIENTED_EDGE('',*,*,#8018,.F.);
#10164=ORIENTED_EDGE('',*,*,#8019,.F.);
#10165=ORIENTED_EDGE('',*,*,#8020,.T.);
#10166=ORIENTED_EDGE('',*,*,#8021,.F.);
#10167=ORIENTED_EDGE('',*,*,#8020,.F.);
#10168=ORIENTED_EDGE('',*,*,#8018,.T.);
#10169=ORIENTED_EDGE('',*,*,#8022,.T.);
#10170=ORIENTED_EDGE('',*,*,#8023,.F.);
#10171=ORIENTED_EDGE('',*,*,#8022,.F.);
#10172=ORIENTED_EDGE('',*,*,#8014,.T.);
#10173=ORIENTED_EDGE('',*,*,#8024,.T.);
#10174=ORIENTED_EDGE('',*,*,#8025,.F.);
#10175=ORIENTED_EDGE('',*,*,#8024,.F.);
#10176=ORIENTED_EDGE('',*,*,#8026,.T.);
#10177=ORIENTED_EDGE('',*,*,#8027,.T.);
#10178=ORIENTED_EDGE('',*,*,#8028,.F.);
#10179=ORIENTED_EDGE('',*,*,#8029,.F.);
#10180=ORIENTED_EDGE('',*,*,#8030,.T.);
#10181=ORIENTED_EDGE('',*,*,#8029,.T.);
#10182=ORIENTED_EDGE('',*,*,#8031,.F.);
#10183=ORIENTED_EDGE('',*,*,#8032,.F.);
#10184=ORIENTED_EDGE('',*,*,#8033,.T.);
#10185=ORIENTED_EDGE('',*,*,#8032,.T.);
#10186=ORIENTED_EDGE('',*,*,#8034,.F.);
#10187=ORIENTED_EDGE('',*,*,#8035,.F.);
#10188=ORIENTED_EDGE('',*,*,#8036,.T.);
#10189=ORIENTED_EDGE('',*,*,#8035,.T.);
#10190=ORIENTED_EDGE('',*,*,#8037,.F.);
#10191=ORIENTED_EDGE('',*,*,#8027,.F.);
#10192=ORIENTED_EDGE('',*,*,#8037,.T.);
#10193=ORIENTED_EDGE('',*,*,#8034,.T.);
#10194=ORIENTED_EDGE('',*,*,#8031,.T.);
#10195=ORIENTED_EDGE('',*,*,#8028,.T.);
#10196=ORIENTED_EDGE('',*,*,#8021,.T.);
#10197=ORIENTED_EDGE('',*,*,#8023,.T.);
#10198=ORIENTED_EDGE('',*,*,#8025,.T.);
#10199=ORIENTED_EDGE('',*,*,#8036,.F.);
#10200=ORIENTED_EDGE('',*,*,#8026,.F.);
#10201=ORIENTED_EDGE('',*,*,#8030,.F.);
#10202=ORIENTED_EDGE('',*,*,#8033,.F.);
#10203=ORIENTED_EDGE('',*,*,#8011,.T.);
#10204=ORIENTED_EDGE('',*,*,#8015,.T.);
#10205=ORIENTED_EDGE('',*,*,#8019,.T.);
#12198=CYLINDRICAL_SURFACE('',#15160,1.04);
#12199=CYLINDRICAL_SURFACE('',#15165,1.04);
#12200=CYLINDRICAL_SURFACE('',#15170,0.65);
#12201=CYLINDRICAL_SURFACE('',#15173,0.8);
#12202=CYLINDRICAL_SURFACE('',#15175,0.8);
#12712=ADVANCED_FACE('',(#2345),#12198,.T.);
#12713=ADVANCED_FACE('',(#2346,#1406),#1791,.F.);
#12714=ADVANCED_FACE('',(#2347),#12199,.T.);
#12715=ADVANCED_FACE('',(#2348,#1407),#1792,.F.);
#12716=ADVANCED_FACE('',(#2349),#12200,.F.);
#12717=ADVANCED_FACE('',(#2350),#12201,.F.);
#12718=ADVANCED_FACE('',(#2351),#12202,.F.);
#12719=ADVANCED_FACE('',(#2352),#1793,.T.);
#12720=ADVANCED_FACE('',(#2353),#1794,.T.);
#12721=ADVANCED_FACE('',(#2354),#1795,.T.);
#12722=ADVANCED_FACE('',(#2355),#1796,.T.);
#12723=ADVANCED_FACE('',(#2356,#1408,#1409,#1410),#1797,.T.);
#12724=ADVANCED_FACE('',(#2357,#1411,#1412,#1413),#1798,.F.);
#13283=CLOSED_SHELL('',(#12712,#12713,#12714,#12715,#12716,#12717,#12718,
#12719,#12720,#12721,#12722,#12723,#12724));
#15159=AXIS2_PLACEMENT_3D('',#22274,#17951,#17952);
#15160=AXIS2_PLACEMENT_3D('',#22275,#17953,#17954);
#15161=AXIS2_PLACEMENT_3D('',#22277,#17955,#17956);
#15162=AXIS2_PLACEMENT_3D('',#22280,#17958,#17959);
#15163=AXIS2_PLACEMENT_3D('',#22281,#17960,#17961);
#15164=AXIS2_PLACEMENT_3D('',#22283,#17962,#17963);
#15165=AXIS2_PLACEMENT_3D('',#22284,#17964,#17965);
#15166=AXIS2_PLACEMENT_3D('',#22286,#17966,#17967);
#15167=AXIS2_PLACEMENT_3D('',#22289,#17969,#17970);
#15168=AXIS2_PLACEMENT_3D('',#22290,#17971,#17972);
#15169=AXIS2_PLACEMENT_3D('',#22292,#17973,#17974);
#15170=AXIS2_PLACEMENT_3D('',#22293,#17975,#17976);
#15171=AXIS2_PLACEMENT_3D('',#22295,#17977,#17978);
#15172=AXIS2_PLACEMENT_3D('',#22298,#17980,#17981);
#15173=AXIS2_PLACEMENT_3D('',#22299,#17982,#17983);
#15174=AXIS2_PLACEMENT_3D('',#22302,#17985,#17986);
#15175=AXIS2_PLACEMENT_3D('',#22303,#17987,#17988);
#15176=AXIS2_PLACEMENT_3D('',#22306,#17990,#17991);
#15177=AXIS2_PLACEMENT_3D('',#22307,#17992,#17993);
#15178=AXIS2_PLACEMENT_3D('',#22316,#17998,#17999);
#15179=AXIS2_PLACEMENT_3D('',#22322,#18003,#18004);
#15180=AXIS2_PLACEMENT_3D('',#22328,#18008,#18009);
#15181=AXIS2_PLACEMENT_3D('',#22331,#18012,#18013);
#15182=AXIS2_PLACEMENT_3D('',#22332,#18014,#18015);
#17951=DIRECTION('axis',(0.,0.,1.));
#17952=DIRECTION('refdir',(1.,0.,0.));
#17953=DIRECTION('center_axis',(1.,0.,0.));
#17954=DIRECTION('ref_axis',(0.,0.,-1.));
#17955=DIRECTION('center_axis',(1.,0.,0.));
#17956=DIRECTION('ref_axis',(0.,0.,-1.));
#17957=DIRECTION('',(-1.,0.,0.));
#17958=DIRECTION('center_axis',(1.,0.,0.));
#17959=DIRECTION('ref_axis',(0.,0.,-1.));
#17960=DIRECTION('center_axis',(1.,0.,0.));
#17961=DIRECTION('ref_axis',(0.,0.,-1.));
#17962=DIRECTION('center_axis',(-1.,0.,0.));
#17963=DIRECTION('ref_axis',(0.,0.,-1.));
#17964=DIRECTION('center_axis',(1.,0.,0.));
#17965=DIRECTION('ref_axis',(0.,0.,-1.));
#17966=DIRECTION('center_axis',(1.,0.,0.));
#17967=DIRECTION('ref_axis',(0.,0.,-1.));
#17968=DIRECTION('',(-1.,0.,0.));
#17969=DIRECTION('center_axis',(1.,0.,0.));
#17970=DIRECTION('ref_axis',(0.,0.,-1.));
#17971=DIRECTION('center_axis',(1.,0.,0.));
#17972=DIRECTION('ref_axis',(0.,0.,-1.));
#17973=DIRECTION('center_axis',(-1.,0.,0.));
#17974=DIRECTION('ref_axis',(0.,0.,-1.));
#17975=DIRECTION('center_axis',(1.,0.,0.));
#17976=DIRECTION('ref_axis',(0.,0.,-1.));
#17977=DIRECTION('center_axis',(1.,0.,0.));
#17978=DIRECTION('ref_axis',(0.,0.,-1.));
#17979=DIRECTION('',(1.,0.,0.));
#17980=DIRECTION('center_axis',(-1.,0.,0.));
#17981=DIRECTION('ref_axis',(0.,0.,-1.));
#17982=DIRECTION('center_axis',(1.,0.,0.));
#17983=DIRECTION('ref_axis',(0.,0.,-1.));
#17984=DIRECTION('',(1.,0.,0.));
#17985=DIRECTION('center_axis',(-1.,0.,0.));
#17986=DIRECTION('ref_axis',(0.,0.,-1.));
#17987=DIRECTION('center_axis',(1.,0.,0.));
#17988=DIRECTION('ref_axis',(0.,0.,-1.));
#17989=DIRECTION('',(1.,0.,0.));
#17990=DIRECTION('center_axis',(-1.,0.,0.));
#17991=DIRECTION('ref_axis',(0.,0.,-1.));
#17992=DIRECTION('center_axis',(0.,0.,1.));
#17993=DIRECTION('ref_axis',(0.,-1.,0.));
#17994=DIRECTION('',(0.,-1.,0.));
#17995=DIRECTION('',(1.,0.,0.));
#17996=DIRECTION('',(0.,-1.,0.));
#17997=DIRECTION('',(1.,0.,0.));
#17998=DIRECTION('center_axis',(0.,1.,0.));
#17999=DIRECTION('ref_axis',(0.,0.,1.));
#18000=DIRECTION('',(0.,0.,1.));
#18001=DIRECTION('',(0.,0.,1.));
#18002=DIRECTION('',(1.,0.,0.));
#18003=DIRECTION('center_axis',(0.,0.,-1.));
#18004=DIRECTION('ref_axis',(0.,1.,0.));
#18005=DIRECTION('',(0.,1.,0.));
#18006=DIRECTION('',(0.,1.,0.));
#18007=DIRECTION('',(1.,0.,0.));
#18008=DIRECTION('center_axis',(0.,-1.,0.));
#18009=DIRECTION('ref_axis',(0.,0.,-1.));
#18010=DIRECTION('',(0.,0.,-1.));
#18011=DIRECTION('',(0.,0.,-1.));
#18012=DIRECTION('center_axis',(1.,0.,0.));
#18013=DIRECTION('ref_axis',(0.,0.,-1.));
#18014=DIRECTION('center_axis',(1.,0.,0.));
#18015=DIRECTION('ref_axis',(0.,0.,-1.));
#22274=CARTESIAN_POINT('',(0.,0.,0.));
#22275=CARTESIAN_POINT('Origin',(40.22983346,3.,6.));
#22276=CARTESIAN_POINT('',(40.42983346,3.,7.04));
#22277=CARTESIAN_POINT('Origin',(40.42983346,3.,6.));
#22278=CARTESIAN_POINT('',(40.22983346,3.,7.04));
#22279=CARTESIAN_POINT('',(40.22983346,3.,7.04));
#22280=CARTESIAN_POINT('Origin',(40.22983346,3.,6.));
#22281=CARTESIAN_POINT('Origin',(40.22983346,3.,6.));
#22282=CARTESIAN_POINT('',(40.22983346,3.,6.8));
#22283=CARTESIAN_POINT('Origin',(40.22983346,3.,6.));
#22284=CARTESIAN_POINT('Origin',(40.22983346,-3.,6.));
#22285=CARTESIAN_POINT('',(40.42983346,-3.,7.04));
#22286=CARTESIAN_POINT('Origin',(40.42983346,-3.,6.));
#22287=CARTESIAN_POINT('',(40.22983346,-3.,7.04));
#22288=CARTESIAN_POINT('',(40.22983346,-3.,7.04));
#22289=CARTESIAN_POINT('Origin',(40.22983346,-3.,6.));
#22290=CARTESIAN_POINT('Origin',(40.22983346,-3.,6.));
#22291=CARTESIAN_POINT('',(40.22983346,-3.,6.8));
#22292=CARTESIAN_POINT('Origin',(40.22983346,-3.,6.));
#22293=CARTESIAN_POINT('Origin',(40.32983346,0.,6.));
#22294=CARTESIAN_POINT('',(40.42983346,-7.9602041944578E-17,6.65));
#22295=CARTESIAN_POINT('Origin',(40.42983346,0.,6.));
#22296=CARTESIAN_POINT('',(40.62983346,7.9602041944578E-17,6.65));
#22297=CARTESIAN_POINT('',(40.32983346,-7.9602041944578E-17,6.65));
#22298=CARTESIAN_POINT('Origin',(40.62983346,0.,6.));
#22299=CARTESIAN_POINT('Origin',(40.32983346,-3.,6.));
#22300=CARTESIAN_POINT('',(40.62983346,-3.,6.8));
#22301=CARTESIAN_POINT('',(40.32983346,-3.,6.8));
#22302=CARTESIAN_POINT('Origin',(40.62983346,-3.,6.));
#22303=CARTESIAN_POINT('Origin',(40.32983346,3.,6.));
#22304=CARTESIAN_POINT('',(40.62983346,3.,6.8));
#22305=CARTESIAN_POINT('',(40.32983346,3.,6.8));
#22306=CARTESIAN_POINT('Origin',(40.62983346,3.,6.));
#22307=CARTESIAN_POINT('Origin',(40.42983346,4.7,7.7));
#22308=CARTESIAN_POINT('',(40.42983346,4.7,7.7));
#22309=CARTESIAN_POINT('',(40.42983346,-4.3,7.7));
#22310=CARTESIAN_POINT('',(40.42983346,4.7,7.7));
#22311=CARTESIAN_POINT('',(40.62983346,-4.3,7.7));
#22312=CARTESIAN_POINT('',(40.42983346,-4.3,7.7));
#22313=CARTESIAN_POINT('',(40.62983346,4.7,7.7));
#22314=CARTESIAN_POINT('',(40.62983346,4.7,7.7));
#22315=CARTESIAN_POINT('',(40.42983346,4.7,7.7));
#22316=CARTESIAN_POINT('Origin',(40.42983346,4.7,4.3));
#22317=CARTESIAN_POINT('',(40.42983346,4.7,4.3));
#22318=CARTESIAN_POINT('',(40.42983346,4.7,4.3));
#22319=CARTESIAN_POINT('',(40.62983346,4.7,4.3));
#22320=CARTESIAN_POINT('',(40.62983346,4.7,4.3));
#22321=CARTESIAN_POINT('',(40.42983346,4.7,4.3));
#22322=CARTESIAN_POINT('Origin',(40.42983346,-4.3,4.3));
#22323=CARTESIAN_POINT('',(40.42983346,-4.3,4.3));
#22324=CARTESIAN_POINT('',(40.42983346,-4.3,4.3));
#22325=CARTESIAN_POINT('',(40.62983346,-4.3,4.3));
#22326=CARTESIAN_POINT('',(40.62983346,-4.3,4.3));
#22327=CARTESIAN_POINT('',(40.42983346,-4.3,4.3));
#22328=CARTESIAN_POINT('Origin',(40.42983346,-4.3,7.7));
#22329=CARTESIAN_POINT('',(40.42983346,-4.3,7.7));
#22330=CARTESIAN_POINT('',(40.62983346,-4.3,7.7));
#22331=CARTESIAN_POINT('Origin',(40.62983346,0.2,6.));
#22332=CARTESIAN_POINT('Origin',(40.42983346,0.2,6.));
#24896=UNCERTAINTY_MEASURE_WITH_UNIT(LENGTH_MEASURE(0.001),#25101,
'DISTANCE_ACCURACY_VALUE',
'Maximum model space distance between geometric entities at asserted c
onnectivities');
#24979=UNCERTAINTY_MEASURE_WITH_UNIT(LENGTH_MEASURE(0.001),#25101,
'DISTANCE_ACCURACY_VALUE',
'Maximum model space distance between geometric entities at asserted c
onnectivities');
#25017=(
GEOMETRIC_REPRESENTATION_CONTEXT(3)
GLOBAL_UNCERTAINTY_ASSIGNED_CONTEXT((#24896))
GLOBAL_UNIT_ASSIGNED_CONTEXT((#25101,#25103,#25104))
REPRESENTATION_CONTEXT('','3D')
);
#25100=(
GEOMETRIC_REPRESENTATION_CONTEXT(3)
GLOBAL_UNCERTAINTY_ASSIGNED_CONTEXT((#24979))
GLOBAL_UNIT_ASSIGNED_CONTEXT((#25101,#25103,#25104))
REPRESENTATION_CONTEXT('','3D')
);
#25101=(
LENGTH_UNIT()
NAMED_UNIT(*)
SI_UNIT(.CENTI.,.METRE.)
);
#25103=(
NAMED_UNIT(*)
PLANE_ANGLE_UNIT()
SI_UNIT($,.RADIAN.)
);
#25104=(
NAMED_UNIT(*)
SI_UNIT($,.STERADIAN.)
SOLID_ANGLE_UNIT()
);
#25142=SHAPE_DEFINITION_REPRESENTATION(#25262,#25547);
#25262=PRODUCT_DEFINITION_SHAPE('',$,#25668);
#25547=SHAPE_REPRESENTATION('',(#15159),#25017);
#25630=PRODUCT_DEFINITION_CONTEXT('part definition',#25992,'design');
#25668=PRODUCT_DEFINITION('Linear bearing keeper (1)',
'Linear bearing keeper (1)',#25788,#25630);
#25788=PRODUCT_DEFINITION_FORMATION('',$,#26031);
#25992=APPLICATION_CONTEXT(
'Core Data for Automotive Mechanical Design Process');
#25993=PRODUCT_CONTEXT('part definition',#25992,'mechanical');
#26031=PRODUCT('Linear bearing keeper (1)','Linear bearing keeper (1)',
'Linear bearing keeper (1)',(#25993));
#26185=COLOUR_RGB('Grey',0.48,0.52,0.57);
#26186=FILL_AREA_STYLE_COLOUR('',#26185);
#26187=FILL_AREA_STYLE('',(#26186));
#26188=SURFACE_STYLE_FILL_AREA(#26187);
#26189=SURFACE_SIDE_STYLE('',(#26188));
#26190=SURFACE_STYLE_USAGE(.BOTH.,#26189);
#26191=PRESENTATION_STYLE_ASSIGNMENT((#26190));
ENDSEC;
END-ISO-10303-21;
